ISO-10303-21;
HEADER;
/* Generated by software containing ST-Developer
 * from STEP Tools, Inc. (www.steptools.com) 
 */

FILE_DESCRIPTION(
/* description */ ('STEP AP203'),
/* implementation_level */ '2;1');

FILE_NAME(
/* name */ 'P14_Upper_Feed_Nut.step',
/* time_stamp */ '2026-11-15T15:04:01-08:00',
/* author */ (''),
/* organization */ (''),
/* preprocessor_version */ 'ST-DEVELOPER v20.2',
/* originating_system */ 'Autodesk Translation Framework v15.17.0.0',
/* authorisation */ '');

FILE_SCHEMA (('AUTOMOTIVE_DESIGN { 1 0 10303 214 3 1 1 }'));
ENDSEC;

DATA;
#10=MECHANICAL_DESIGN_GEOMETRIC_PRESENTATION_REPRESENTATION('',(#293),#16598);
#215=SHAPE_REPRESENTATION_RELATIONSHIP('SRR','None',#16709,#239);
#239=ADVANCED_BREP_SHAPE_REPRESENTATION('',(#263),#16585);
#263=MANIFOLD_SOLID_BREP('Body1',#9798);
#293=STYLED_ITEM('',(#16830),#263);
#357=FACE_BOUND('',#1747,.T.);
#358=FACE_BOUND('',#1749,.T.);
#621=PLANE('',#10418);
#622=PLANE('',#10419);
#623=PLANE('',#10420);
#624=PLANE('',#10421);
#625=PLANE('',#10422);
#626=PLANE('',#10423);
#1143=FACE_OUTER_BOUND('',#1745,.T.);
#1144=FACE_OUTER_BOUND('',#1746,.T.);
#1145=FACE_OUTER_BOUND('',#1748,.T.);
#1146=FACE_OUTER_BOUND('',#1750,.T.);
#1147=FACE_OUTER_BOUND('',#1751,.T.);
#1148=FACE_OUTER_BOUND('',#1752,.T.);
#1149=FACE_OUTER_BOUND('',#1753,.T.);
#1745=EDGE_LOOP('',(#7707,#7708,#7709,#7710));
#1746=EDGE_LOOP('',(#7711,#7712,#7713,#7714));
#1747=EDGE_LOOP('',(#7715));
#1748=EDGE_LOOP('',(#7716,#7717,#7718,#7719));
#1749=EDGE_LOOP('',(#7720));
#1750=EDGE_LOOP('',(#7721,#7722,#7723,#7724));
#1751=EDGE_LOOP('',(#7725,#7726,#7727,#7728));
#1752=EDGE_LOOP('',(#7729,#7730,#7731,#7732));
#1753=EDGE_LOOP('',(#7733,#7734,#7735,#7736));
#2593=LINE('',#14924,#3641);
#2594=LINE('',#14929,#3642);
#2595=LINE('',#14931,#3643);
#2596=LINE('',#14933,#3644);
#2597=LINE('',#14934,#3645);
#2598=LINE('',#14938,#3646);
#2599=LINE('',#14940,#3647);
#2600=LINE('',#14942,#3648);
#2601=LINE('',#14943,#3649);
#2602=LINE('',#14945,#3650);
#2603=LINE('',#14946,#3651);
#2604=LINE('',#14948,#3652);
#2605=LINE('',#14950,#3653);
#3641=VECTOR('',#12067,7.35);
#3642=VECTOR('',#12072,1000.);
#3643=VECTOR('',#12073,1000.);
#3644=VECTOR('',#12074,1000.);
#3645=VECTOR('',#12075,1000.);
#3646=VECTOR('',#12078,1000.);
#3647=VECTOR('',#12079,1000.);
#3648=VECTOR('',#12080,1000.);
#3649=VECTOR('',#12081,1000.);
#3650=VECTOR('',#12084,1000.);
#3651=VECTOR('',#12085,1000.);
#3652=VECTOR('',#12088,1000.);
#3653=VECTOR('',#12091,1000.);
#4317=CIRCLE('',#10416,7.35);
#4318=CIRCLE('',#10417,7.35);
#4825=VERTEX_POINT('',#14921);
#4826=VERTEX_POINT('',#14923);
#4827=VERTEX_POINT('',#14927);
#4828=VERTEX_POINT('',#14928);
#4829=VERTEX_POINT('',#14930);
#4830=VERTEX_POINT('',#14932);
#4831=VERTEX_POINT('',#14936);
#4832=VERTEX_POINT('',#14937);
#4833=VERTEX_POINT('',#14939);
#4834=VERTEX_POINT('',#14941);
#5866=EDGE_CURVE('',#4825,#4825,#4317,.T.);
#5867=EDGE_CURVE('',#4825,#4826,#2593,.T.);
#5868=EDGE_CURVE('',#4826,#4826,#4318,.T.);
#5869=EDGE_CURVE('',#4827,#4828,#2594,.T.);
#5870=EDGE_CURVE('',#4828,#4829,#2595,.T.);
#5871=EDGE_CURVE('',#4829,#4830,#2596,.T.);
#5872=EDGE_CURVE('',#4830,#4827,#2597,.T.);
#5873=EDGE_CURVE('',#4831,#4832,#2598,.T.);
#5874=EDGE_CURVE('',#4833,#4831,#2599,.T.);
#5875=EDGE_CURVE('',#4834,#4833,#2600,.T.);
#5876=EDGE_CURVE('',#4832,#4834,#2601,.T.);
#5877=EDGE_CURVE('',#4828,#4832,#2602,.T.);
#5878=EDGE_CURVE('',#4827,#4831,#2603,.T.);
#5879=EDGE_CURVE('',#4829,#4834,#2604,.T.);
#5880=EDGE_CURVE('',#4830,#4833,#2605,.T.);
#7707=ORIENTED_EDGE('',*,*,#5866,.T.);
#7708=ORIENTED_EDGE('',*,*,#5867,.T.);
#7709=ORIENTED_EDGE('',*,*,#5868,.F.);
#7710=ORIENTED_EDGE('',*,*,#5867,.F.);
#7711=ORIENTED_EDGE('',*,*,#5869,.T.);
#7712=ORIENTED_EDGE('',*,*,#5870,.T.);
#7713=ORIENTED_EDGE('',*,*,#5871,.T.);
#7714=ORIENTED_EDGE('',*,*,#5872,.T.);
#7715=ORIENTED_EDGE('',*,*,#5866,.F.);
#7716=ORIENTED_EDGE('',*,*,#5873,.F.);
#7717=ORIENTED_EDGE('',*,*,#5874,.F.);
#7718=ORIENTED_EDGE('',*,*,#5875,.F.);
#7719=ORIENTED_EDGE('',*,*,#5876,.F.);
#7720=ORIENTED_EDGE('',*,*,#5868,.T.);
#7721=ORIENTED_EDGE('',*,*,#5873,.T.);
#7722=ORIENTED_EDGE('',*,*,#5877,.F.);
#7723=ORIENTED_EDGE('',*,*,#5869,.F.);
#7724=ORIENTED_EDGE('',*,*,#5878,.T.);
#7725=ORIENTED_EDGE('',*,*,#5876,.T.);
#7726=ORIENTED_EDGE('',*,*,#5879,.F.);
#7727=ORIENTED_EDGE('',*,*,#5870,.F.);
#7728=ORIENTED_EDGE('',*,*,#5877,.T.);
#7729=ORIENTED_EDGE('',*,*,#5875,.T.);
#7730=ORIENTED_EDGE('',*,*,#5880,.F.);
#7731=ORIENTED_EDGE('',*,*,#5871,.F.);
#7732=ORIENTED_EDGE('',*,*,#5879,.T.);
#7733=ORIENTED_EDGE('',*,*,#5874,.T.);
#7734=ORIENTED_EDGE('',*,*,#5878,.F.);
#7735=ORIENTED_EDGE('',*,*,#5872,.F.);
#7736=ORIENTED_EDGE('',*,*,#5880,.T.);
#9209=CYLINDRICAL_SURFACE('',#10415,7.35);
#9468=ADVANCED_FACE('',(#1143),#9209,.F.);
#9469=ADVANCED_FACE('',(#1144,#357),#621,.T.);
#9470=ADVANCED_FACE('',(#1145,#358),#622,.F.);
#9471=ADVANCED_FACE('',(#1146),#623,.F.);
#9472=ADVANCED_FACE('',(#1147),#624,.F.);
#9473=ADVANCED_FACE('',(#1148),#625,.F.);
#9474=ADVANCED_FACE('',(#1149),#626,.F.);
#9798=CLOSED_SHELL('',(#9468,#9469,#9470,#9471,#9472,#9473,#9474));
#10414=AXIS2_PLACEMENT_3D('',#14919,#12061,#12062);
#10415=AXIS2_PLACEMENT_3D('',#14920,#12063,#12064);
#10416=AXIS2_PLACEMENT_3D('',#14922,#12065,#12066);
#10417=AXIS2_PLACEMENT_3D('',#14925,#12068,#12069);
#10418=AXIS2_PLACEMENT_3D('',#14926,#12070,#12071);
#10419=AXIS2_PLACEMENT_3D('',#14935,#12076,#12077);
#10420=AXIS2_PLACEMENT_3D('',#14944,#12082,#12083);
#10421=AXIS2_PLACEMENT_3D('',#14947,#12086,#12087);
#10422=AXIS2_PLACEMENT_3D('',#14949,#12089,#12090);
#10423=AXIS2_PLACEMENT_3D('',#14951,#12092,#12093);
#12061=DIRECTION('axis',(0.,0.,1.));
#12062=DIRECTION('refdir',(1.,0.,0.));
#12063=DIRECTION('center_axis',(0.,-1.,0.));
#12064=DIRECTION('ref_axis',(0.,0.,-1.));
#12065=DIRECTION('center_axis',(0.,1.,0.));
#12066=DIRECTION('ref_axis',(0.,0.,1.));
#12067=DIRECTION('',(0.,-1.,0.));
#12068=DIRECTION('center_axis',(0.,1.,0.));
#12069=DIRECTION('ref_axis',(0.,0.,1.));
#12070=DIRECTION('center_axis',(0.,1.,0.));
#12071=DIRECTION('ref_axis',(0.,0.,1.));
#12072=DIRECTION('',(0.,0.,-1.));
#12073=DIRECTION('',(-1.,0.,0.));
#12074=DIRECTION('',(0.,0.,1.));
#12075=DIRECTION('',(1.,0.,0.));
#12076=DIRECTION('center_axis',(0.,1.,0.));
#12077=DIRECTION('ref_axis',(0.,0.,1.));
#12078=DIRECTION('',(0.,0.,-1.));
#12079=DIRECTION('',(1.,0.,0.));
#12080=DIRECTION('',(0.,0.,1.));
#12081=DIRECTION('',(-1.,0.,0.));
#12082=DIRECTION('center_axis',(-1.,0.,0.));
#12083=DIRECTION('ref_axis',(0.,0.,1.));
#12084=DIRECTION('',(0.,-1.,0.));
#12085=DIRECTION('',(0.,-1.,0.));
#12086=DIRECTION('center_axis',(0.,0.,1.));
#12087=DIRECTION('ref_axis',(1.,0.,0.));
#12088=DIRECTION('',(0.,-1.,0.));
#12089=DIRECTION('center_axis',(1.,0.,0.));
#12090=DIRECTION('ref_axis',(0.,0.,-1.));
#12091=DIRECTION('',(0.,-1.,0.));
#12092=DIRECTION('center_axis',(0.,0.,-1.));
#12093=DIRECTION('ref_axis',(-1.,0.,0.));
#14919=CARTESIAN_POINT('',(0.,0.,0.));
#14920=CARTESIAN_POINT('Origin',(0.,12.,55.));
#14921=CARTESIAN_POINT('',(-9.00115397373305E-16,12.,62.35));
#14922=CARTESIAN_POINT('Origin',(0.,12.,55.));
#14923=CARTESIAN_POINT('',(-9.00115397373305E-16,-12.,62.35));
#14924=CARTESIAN_POINT('',(-9.00115397373305E-16,12.,62.35));
#14925=CARTESIAN_POINT('Origin',(0.,-12.,55.));
#14926=CARTESIAN_POINT('Origin',(0.,12.,0.));
#14927=CARTESIAN_POINT('',(11.,12.,68.3));
#14928=CARTESIAN_POINT('',(11.,12.,44.3));
#14929=CARTESIAN_POINT('',(11.,12.,44.3));
#14930=CARTESIAN_POINT('',(-11.,12.,44.3));
#14931=CARTESIAN_POINT('',(-11.,12.,44.3));
#14932=CARTESIAN_POINT('',(-11.,12.,68.3));
#14933=CARTESIAN_POINT('',(-11.,12.,44.3));
#14934=CARTESIAN_POINT('',(-11.,12.,68.3));
#14935=CARTESIAN_POINT('Origin',(0.,-12.,0.));
#14936=CARTESIAN_POINT('',(11.,-12.,68.3));
#14937=CARTESIAN_POINT('',(11.,-12.,44.3));
#14938=CARTESIAN_POINT('',(11.,-12.,44.3));
#14939=CARTESIAN_POINT('',(-11.,-12.,68.3));
#14940=CARTESIAN_POINT('',(-11.,-12.,68.3));
#14941=CARTESIAN_POINT('',(-11.,-12.,44.3));
#14942=CARTESIAN_POINT('',(-11.,-12.,44.3));
#14943=CARTESIAN_POINT('',(-11.,-12.,44.3));
#14944=CARTESIAN_POINT('Origin',(11.,12.,44.3));
#14945=CARTESIAN_POINT('',(11.,12.,44.3));
#14946=CARTESIAN_POINT('',(11.,12.,68.3));
#14947=CARTESIAN_POINT('Origin',(-11.,12.,44.3));
#14948=CARTESIAN_POINT('',(-11.,12.,44.3));
#14949=CARTESIAN_POINT('Origin',(-11.,12.,44.3));
#14950=CARTESIAN_POINT('',(-11.,12.,68.3));
#14951=CARTESIAN_POINT('Origin',(-11.,12.,68.3));
#16559=UNCERTAINTY_MEASURE_WITH_UNIT(LENGTH_MEASURE(0.01),#16599,
'DISTANCE_ACCURACY_VALUE',
'Maximum model space distance between geometric entities at asserted c
onnectivities');
#16572=UNCERTAINTY_MEASURE_WITH_UNIT(LENGTH_MEASURE(0.01),#16599,
'DISTANCE_ACCURACY_VALUE',
'Maximum model space distance between geometric entities at asserted c
onnectivities');
#16585=(
GEOMETRIC_REPRESENTATION_CONTEXT(3)
GLOBAL_UNCERTAINTY_ASSIGNED_CONTEXT((#16559))
GLOBAL_UNIT_ASSIGNED_CONTEXT((#16599,#16601,#16602))
REPRESENTATION_CONTEXT('','3D')
);
#16598=(
GEOMETRIC_REPRESENTATION_CONTEXT(3)
GLOBAL_UNCERTAINTY_ASSIGNED_CONTEXT((#16572))
GLOBAL_UNIT_ASSIGNED_CONTEXT((#16599,#16601,#16602))
REPRESENTATION_CONTEXT('','3D')
);
#16599=(
LENGTH_UNIT()
NAMED_UNIT(*)
SI_UNIT(.MILLI.,.METRE.)
);
#16601=(
NAMED_UNIT(*)
PLANE_ANGLE_UNIT()
SI_UNIT($,.RADIAN.)
);
#16602=(
NAMED_UNIT(*)
SI_UNIT($,.STERADIAN.)
SOLID_ANGLE_UNIT()
);
#16615=SHAPE_DEFINITION_REPRESENTATION(#16640,#16709);
#16640=PRODUCT_DEFINITION_SHAPE('',$,#16735);
#16709=SHAPE_REPRESENTATION('',(#10414),#16585);
#16722=PRODUCT_DEFINITION_CONTEXT('part definition',#16799,'design');
#16735=PRODUCT_DEFINITION('P14_Upper_Feed_Nut','P14_Upper_Feed_Nut',#16760,
#16722);
#16760=PRODUCT_DEFINITION_FORMATION('',$,#16813);
#16799=APPLICATION_CONTEXT(
'Core Data for Automotive Mechanical Design Process');
#16800=PRODUCT_CONTEXT('part definition',#16799,'mechanical');
#16813=PRODUCT('P14_Upper_Feed_Nut','P14_Upper_Feed_Nut',$,(#16800));
#16830=PRESENTATION_STYLE_ASSIGNMENT((#16839));
#16839=SURFACE_STYLE_USAGE(.BOTH.,#16848);
#16848=SURFACE_SIDE_STYLE('',(#16857));
#16857=SURFACE_STYLE_FILL_AREA(#16866);
#16866=FILL_AREA_STYLE('Dark Blue',(#16875));
#16875=FILL_AREA_STYLE_COLOUR('Dark Blue',#16884);
#16884=COLOUR_RGB('Dark Blue',0.,0.125490196078431,0.376470588235294);
ENDSEC;
END-ISO-10303-21;
